ISO-10303-21;
HEADER;
FILE_DESCRIPTION (('STEP AP214'),
    '1' );
FILE_NAME ('Part 134_Varsay\X2\0131\X0\lan.step',
    '2026-10-08T11:03:28',
    ( '' ),
    ( '' ),
    'SwSTEP 2.0',
    'SolidWorks 2024',
    '' );
FILE_SCHEMA (( 'AUTOMOTIVE_DESIGN' ));
ENDSEC;

DATA;
#3=ORIENTED_EDGE ( 'NONE', *, *, #1718, .F. ) ;
#55=DIRECTION ( 'NONE',  ( -0.000000000000000000, -0.000000000000000000, -1.000000000000000000 ) ) ;
#129=DIRECTION ( 'NONE',  ( 0.000000000000000000, 0.000000000000000000, 1.000000000000000000 ) ) ;
#137=DIRECTION ( 'NONE',  ( -1.000000000000000000, 0.000000000000000000, 0.000000000000000000 ) ) ;
#153=LINE ( 'NONE', #555, #974 ) ;
#178=CIRCLE ( 'NONE', #3931, 3.573749999999998650 ) ;
#185=EDGE_CURVE ( 'NONE', #3472, #4004, #3811, .T. ) ;
#187=EDGE_LOOP ( 'NONE', ( #3, #2637, #1708, #1494 ) ) ;
#323=ADVANCED_BREP_SHAPE_REPRESENTATION ( '', ( #3432, #4483 ), #3865 ) ;
#324=APPLICATION_CONTEXT ( 'automotive_design' ) ;
#400=CARTESIAN_POINT ( 'NONE',  ( 2.316727177394501718E-17, 0.000000000000000000, 33.33750000000000568 ) ) ;
#457=( LENGTH_UNIT ( ) NAMED_UNIT ( * ) SI_UNIT ( .MILLI., .METRE. ) );
#477=EDGE_LOOP ( 'NONE', ( #2137, #523 ) ) ;
#523=ORIENTED_EDGE ( 'NONE', *, *, #3458, .F. ) ;
#530=DIRECTION ( 'NONE',  ( 1.000000000000000000, 0.000000000000000000, 0.000000000000000000 ) ) ;
#540=STYLED_ITEM ( 'NONE', ( #3656 ), #3432 ) ;
#549=ORIENTED_EDGE ( 'NONE', *, *, #3023, .T. ) ;
#555=CARTESIAN_POINT ( 'NONE',  ( 3.573749999999998650, 4.376581498452851814E-16, 33.33750000000000568 ) ) ;
#638=CLOSED_SHELL ( 'NONE', ( #3107, #3851, #4206, #671 ) ) ;
#671=ADVANCED_FACE ( 'NONE', ( #3174 ), #2134, .F. ) ;
#702=EDGE_LOOP ( 'NONE', ( #2986, #2462, #3719, #3899 ) ) ;
#758=PRODUCT_CONTEXT ( 'NONE', #324, 'mechanical' ) ;
#777=CARTESIAN_POINT ( 'NONE',  ( 2.316727177394501718E-17, 0.000000000000000000, 33.33750000000000568 ) ) ;
#787=PRODUCT_DEFINITION_FORMATION_WITH_SPECIFIED_SOURCE ( 'ANY', '', #4598, .NOT_KNOWN. ) ;
#809=SURFACE_STYLE_FILL_AREA ( #1922 ) ;
#816=CARTESIAN_POINT ( 'NONE',  ( 2.316727177394501718E-17, 0.000000000000000000, 33.33750000000000568 ) ) ;
#858=( NAMED_UNIT ( * ) PLANE_ANGLE_UNIT ( ) SI_UNIT ( $, .RADIAN. ) );
#911=AXIS2_PLACEMENT_3D ( 'NONE', #1773, #1007, #4275 ) ;
#974=VECTOR ( 'NONE', #1575, 1000.000000000000000 ) ;
#1007=DIRECTION ( 'NONE',  ( 0.000000000000000000, 0.000000000000000000, 1.000000000000000000 ) ) ;
#1057=CARTESIAN_POINT ( 'NONE',  ( 3.573749999999998650, 4.376581498452851814E-16, 4.762500000000001066 ) ) ;
#1166=DIRECTION ( 'NONE',  ( -0.000000000000000000, -0.000000000000000000, -1.000000000000000000 ) ) ;
#1199=AXIS2_PLACEMENT_3D ( 'NONE', #816, #1930, #3731 ) ;
#1283=VERTEX_POINT ( 'NONE', #1057 ) ;
#1292=UNCERTAINTY_MEASURE_WITH_UNIT (LENGTH_MEASURE( 1.000000000000000082E-05 ), #457, 'distance_accuracy_value', 'NONE');
#1364=( LENGTH_UNIT ( ) NAMED_UNIT ( * ) SI_UNIT ( .MILLI., .METRE. ) );
#1402=DIRECTION ( 'NONE',  ( 0.000000000000000000, 0.000000000000000000, 1.000000000000000000 ) ) ;
#1434=SHAPE_DEFINITION_REPRESENTATION ( #2441, #1824 ) ;
#1494=ORIENTED_EDGE ( 'NONE', *, *, #2900, .T. ) ;
#1528=COLOUR_RGB ( '', 0.09019608, 0.27058824, 0.51372549) ;
#1575=DIRECTION ( 'NONE',  ( -0.000000000000000000, -0.000000000000000000, -1.000000000000000000 ) ) ;
#1708=ORIENTED_EDGE ( 'NONE', *, *, #2273, .T. ) ;
#1718=EDGE_CURVE ( 'NONE', #3472, #1283, #153, .T. ) ;
#1773=CARTESIAN_POINT ( 'NONE',  ( 2.316727177394501718E-17, 0.000000000000000000, 4.762500000000001066 ) ) ;
#1780=CARTESIAN_POINT ( 'NONE',  ( -3.573749999999998650, 0.000000000000000000, 33.33750000000000568 ) ) ;
#1824=SHAPE_REPRESENTATION ( 'Part 134_Varsay\X2\0131\X0\lan', ( #4483 ), #3865 ) ;
#1900=SURFACE_SIDE_STYLE ('',( #809 ) ) ;
#1922=FILL_AREA_STYLE ('',( #2968 ) ) ;
#1930=DIRECTION ( 'NONE',  ( 0.000000000000000000, 0.000000000000000000, 1.000000000000000000 ) ) ;
#1949=CARTESIAN_POINT ( 'NONE',  ( 3.573749999999998650, 4.376581498452851814E-16, 33.33750000000000568 ) ) ;
#2018=( NAMED_UNIT ( * ) PLANE_ANGLE_UNIT ( ) SI_UNIT ( $, .RADIAN. ) );
#2119=CARTESIAN_POINT ( 'NONE',  ( -3.573749999999998650, 0.000000000000000000, 4.762500000000001066 ) ) ;
#2125=LINE ( 'NONE', #1780, #3439 ) ;
#2134=PLANE ( 'NONE',  #911 ) ;
#2137=ORIENTED_EDGE ( 'NONE', *, *, #2900, .F. ) ;
#2239=CYLINDRICAL_SURFACE ( 'NONE', #2458, 3.573749999999998650 ) ;
#2273=EDGE_CURVE ( 'NONE', #4004, #2998, #2125, .T. ) ;
#2397=CIRCLE ( 'NONE', #3393, 3.573749999999998650 ) ;
#2413=CARTESIAN_POINT ( 'NONE',  ( 2.316727177394501718E-17, 0.000000000000000000, 4.762500000000001066 ) ) ;
#2430=CARTESIAN_POINT ( 'NONE',  ( -3.573749999999998650, 0.000000000000000000, 33.33750000000000568 ) ) ;
#2441=PRODUCT_DEFINITION_SHAPE ( 'NONE', 'NONE',  #3981 ) ;
#2446=AXIS2_PLACEMENT_3D ( 'NONE', #2413, #3443, #2704 ) ;
#2458=AXIS2_PLACEMENT_3D ( 'NONE', #777, #55, #3305 ) ;
#2462=ORIENTED_EDGE ( 'NONE', *, *, #1718, .T. ) ;
#2495=AXIS2_PLACEMENT_3D ( 'NONE', #4380, #1166, #137 ) ;
#2561=( GEOMETRIC_REPRESENTATION_CONTEXT ( 3 ) GLOBAL_UNCERTAINTY_ASSIGNED_CONTEXT ( ( #1292 ) ) GLOBAL_UNIT_ASSIGNED_CONTEXT ( ( #457, #858, #3724 ) ) REPRESENTATION_CONTEXT ( 'NONE', 'WORKASPACE' ) );
#2619=DIRECTION ( 'NONE',  ( 0.000000000000000000, 0.000000000000000000, 1.000000000000000000 ) ) ;
#2637=ORIENTED_EDGE ( 'NONE', *, *, #3023, .F. ) ;
#2704=DIRECTION ( 'NONE',  ( 1.000000000000000000, 0.000000000000000000, 0.000000000000000000 ) ) ;
#2784=MECHANICAL_DESIGN_GEOMETRIC_PRESENTATION_REPRESENTATION('',(#540),#2561);
#2900=EDGE_CURVE ( 'NONE', #2998, #1283, #4493, .T. ) ;
#2968=FILL_AREA_STYLE_COLOUR ( '', #1528 ) ;
#2986=ORIENTED_EDGE ( 'NONE', *, *, #185, .F. ) ;
#2998=VERTEX_POINT ( 'NONE', #2119 ) ;
#3003=ORIENTED_EDGE ( 'NONE', *, *, #185, .T. ) ;
#3006=PRODUCT_DEFINITION_CONTEXT ( 'detailed design', #4320, 'design' ) ;
#3023=EDGE_CURVE ( 'NONE', #4004, #3472, #178, .T. ) ;
#3107=ADVANCED_FACE ( 'NONE', ( #3713 ), #3689, .T. ) ;
#3174=FACE_OUTER_BOUND ( 'NONE', #477, .T. ) ;
#3305=DIRECTION ( 'NONE',  ( -1.000000000000000000, 0.000000000000000000, 0.000000000000000000 ) ) ;
#3348=DIRECTION ( 'NONE',  ( 1.000000000000000000, 0.000000000000000000, 0.000000000000000000 ) ) ;
#3393=AXIS2_PLACEMENT_3D ( 'NONE', #4011, #2619, #530 ) ;
#3432=MANIFOLD_SOLID_BREP ( 'Ölçek1', #638 ) ;
#3439=VECTOR ( 'NONE', #4382, 1000.000000000000000 ) ;
#3443=DIRECTION ( 'NONE',  ( 0.000000000000000000, 0.000000000000000000, 1.000000000000000000 ) ) ;
#3458=EDGE_CURVE ( 'NONE', #1283, #2998, #2397, .T. ) ;
#3472=VERTEX_POINT ( 'NONE', #1949 ) ;
#3656=PRESENTATION_STYLE_ASSIGNMENT (( #4033 ) ) ;
#3689=CYLINDRICAL_SURFACE ( 'NONE', #2495, 3.573749999999998650 ) ;
#3701=DIRECTION ( 'NONE',  ( 0.000000000000000000, 0.000000000000000000, 1.000000000000000000 ) ) ;
#3704=DIRECTION ( 'NONE',  ( 1.000000000000000000, 0.000000000000000000, 0.000000000000000000 ) ) ;
#3713=FACE_OUTER_BOUND ( 'NONE', #702, .T. ) ;
#3719=ORIENTED_EDGE ( 'NONE', *, *, #3458, .T. ) ;
#3724=( NAMED_UNIT ( * ) SI_UNIT ( $, .STERADIAN. ) SOLID_ANGLE_UNIT ( ) );
#3731=DIRECTION ( 'NONE',  ( 1.000000000000000000, 0.000000000000000000, -0.000000000000000000 ) ) ;
#3752=CARTESIAN_POINT ( 'NONE',  ( 0.000000000000000000, 0.000000000000000000, 0.000000000000000000 ) ) ;
#3811=CIRCLE ( 'NONE', #4414, 3.573749999999998650 ) ;
#3851=ADVANCED_FACE ( 'NONE', ( #4500 ), #2239, .T. ) ;
#3865=( GEOMETRIC_REPRESENTATION_CONTEXT ( 3 ) GLOBAL_UNCERTAINTY_ASSIGNED_CONTEXT ( ( #4485 ) ) GLOBAL_UNIT_ASSIGNED_CONTEXT ( ( #1364, #2018, #4243 ) ) REPRESENTATION_CONTEXT ( 'NONE', 'WORKASPACE' ) );
#3899=ORIENTED_EDGE ( 'NONE', *, *, #2273, .F. ) ;
#3925=DIRECTION ( 'NONE',  ( 1.000000000000000000, 0.000000000000000000, 0.000000000000000000 ) ) ;
#3931=AXIS2_PLACEMENT_3D ( 'NONE', #400, #1402, #3925 ) ;
#3981=PRODUCT_DEFINITION ( 'UNKNOWN', '', #787, #3006 ) ;
#4004=VERTEX_POINT ( 'NONE', #2430 ) ;
#4011=CARTESIAN_POINT ( 'NONE',  ( 2.316727177394501718E-17, 0.000000000000000000, 4.762500000000001066 ) ) ;
#4033=SURFACE_STYLE_USAGE ( .BOTH. , #1900 ) ;
#4063=FACE_OUTER_BOUND ( 'NONE', #4286, .T. ) ;
#4102=CARTESIAN_POINT ( 'NONE',  ( 2.316727177394501718E-17, 0.000000000000000000, 33.33750000000000568 ) ) ;
#4155=SHAPE_REPRESENTATION_RELATIONSHIP ( 'NONE' , 'NONE' ,  #1824, #323 ) ;
#4206=ADVANCED_FACE ( 'NONE', ( #4063 ), #4445, .T. ) ;
#4243=( NAMED_UNIT ( * ) SI_UNIT ( $, .STERADIAN. ) SOLID_ANGLE_UNIT ( ) );
#4275=DIRECTION ( 'NONE',  ( 1.000000000000000000, 0.000000000000000000, -0.000000000000000000 ) ) ;
#4286=EDGE_LOOP ( 'NONE', ( #549, #3003 ) ) ;
#4320=APPLICATION_CONTEXT ( 'automotive_design' ) ;
#4380=CARTESIAN_POINT ( 'NONE',  ( 2.316727177394501718E-17, 0.000000000000000000, 33.33750000000000568 ) ) ;
#4382=DIRECTION ( 'NONE',  ( -0.000000000000000000, -0.000000000000000000, -1.000000000000000000 ) ) ;
#4414=AXIS2_PLACEMENT_3D ( 'NONE', #4102, #3701, #3348 ) ;
#4445=PLANE ( 'NONE',  #1199 ) ;
#4483=AXIS2_PLACEMENT_3D ( 'NONE', #3752, #129, #3704 ) ;
#4485=UNCERTAINTY_MEASURE_WITH_UNIT (LENGTH_MEASURE( 1.000000000000000082E-05 ), #1364, 'distance_accuracy_value', 'NONE');
#4493=CIRCLE ( 'NONE', #2446, 3.573749999999998650 ) ;
#4500=FACE_OUTER_BOUND ( 'NONE', #187, .T. ) ;
#4598=PRODUCT ( 'Part 134_Varsay\X2\0131\X0\lan', 'Part 134_Varsay\X2\0131\X0\lan', '', ( #758 ) ) ;
ENDSEC;
END-ISO-10303-21;
